ISO-10303-21;
HEADER;
/* Generated by software containing ST-Developer
 * from STEP Tools, Inc. (www.steptools.com) 
 */

FILE_DESCRIPTION(
/* description */ ('Lever-operated bar clamp (toggle)'),
/* implementation_level */ '2;1');

FILE_NAME(
/* name */ 'M5x14 Cap Screw.step',
/* time_stamp */ '2026-10-28T03:25:02-07:00',
/* author */ (''),
/* organization */ (''),
/* preprocessor_version */ 'ST-DEVELOPER v20.2',
/* originating_system */ 'Autodesk Translation Framework v15.17.0.0',
/* authorisation */ '');

FILE_SCHEMA (('AUTOMOTIVE_DESIGN { 1 0 10303 214 3 1 1 }'));
ENDSEC;

DATA;
#10=MECHANICAL_DESIGN_GEOMETRIC_PRESENTATION_REPRESENTATION('',(#421),#12413);
#305=CONICAL_SURFACE('',#7316,0.4,0.785398163397448);
#306=CONICAL_SURFACE('',#7320,0.41,0.785398163397448);
#307=CONICAL_SURFACE('',#7324,0.26,0.463647609000806);
#326=ORIENTED_CLOSED_SHELL('',*,#6580,.F.);
#330=BREP_WITH_VOIDS('Body1',#6581,(#326));
#345=SHAPE_REPRESENTATION_RELATIONSHIP('SRR','None',#12584,#383);
#383=ADVANCED_BREP_SHAPE_REPRESENTATION('',(#330),#12381);
#421=STYLED_ITEM('',(#12876),#330);
#587=FACE_BOUND('',#1530,.T.);
#728=PLANE('',#7304);
#729=PLANE('',#7305);
#730=PLANE('',#7306);
#731=PLANE('',#7307);
#732=PLANE('',#7308);
#733=PLANE('',#7309);
#734=PLANE('',#7310);
#735=PLANE('',#7311);
#736=PLANE('',#7312);
#737=PLANE('',#7314);
#738=PLANE('',#7322);
#1023=FACE_OUTER_BOUND('',#1516,.T.);
#1024=FACE_OUTER_BOUND('',#1517,.T.);
#1025=FACE_OUTER_BOUND('',#1518,.T.);
#1026=FACE_OUTER_BOUND('',#1519,.T.);
#1027=FACE_OUTER_BOUND('',#1520,.T.);
#1028=FACE_OUTER_BOUND('',#1521,.T.);
#1029=FACE_OUTER_BOUND('',#1522,.T.);
#1030=FACE_OUTER_BOUND('',#1523,.T.);
#1031=FACE_OUTER_BOUND('',#1524,.T.);
#1032=FACE_OUTER_BOUND('',#1525,.T.);
#1033=FACE_OUTER_BOUND('',#1526,.T.);
#1034=FACE_OUTER_BOUND('',#1527,.T.);
#1035=FACE_OUTER_BOUND('',#1528,.T.);
#1036=FACE_OUTER_BOUND('',#1529,.T.);
#1037=FACE_OUTER_BOUND('',#1531,.T.);
#1038=FACE_OUTER_BOUND('',#1532,.T.);
#1516=EDGE_LOOP('',(#4985,#4986,#4987,#4988));
#1517=EDGE_LOOP('',(#4989,#4990,#4991,#4992));
#1518=EDGE_LOOP('',(#4993,#4994,#4995,#4996));
#1519=EDGE_LOOP('',(#4997,#4998,#4999,#5000));
#1520=EDGE_LOOP('',(#5001,#5002,#5003,#5004));
#1521=EDGE_LOOP('',(#5005,#5006,#5007,#5008));
#1522=EDGE_LOOP('',(#5009,#5010,#5011,#5012,#5013,#5014));
#1523=EDGE_LOOP('',(#5015,#5016,#5017,#5018,#5019,#5020));
#1524=EDGE_LOOP('',(#5021));
#1525=EDGE_LOOP('',(#5022));
#1526=EDGE_LOOP('',(#5023,#5024,#5025,#5026));
#1527=EDGE_LOOP('',(#5027,#5028,#5029,#5030));
#1528=EDGE_LOOP('',(#5031,#5032,#5033,#5034));
#1529=EDGE_LOOP('',(#5035));
#1530=EDGE_LOOP('',(#5036));
#1531=EDGE_LOOP('',(#5037,#5038,#5039,#5040));
#1532=EDGE_LOOP('',(#5041,#5042,#5043,#5044));
#2017=LINE('',#10667,#2458);
#2018=LINE('',#10669,#2459);
#2019=LINE('',#10671,#2460);
#2020=LINE('',#10672,#2461);
#2021=LINE('',#10675,#2462);
#2022=LINE('',#10677,#2463);
#2023=LINE('',#10678,#2464);
#2024=LINE('',#10681,#2465);
#2025=LINE('',#10683,#2466);
#2026=LINE('',#10684,#2467);
#2027=LINE('',#10687,#2468);
#2028=LINE('',#10689,#2469);
#2029=LINE('',#10690,#2470);
#2030=LINE('',#10693,#2471);
#2031=LINE('',#10695,#2472);
#2032=LINE('',#10696,#2473);
#2033=LINE('',#10698,#2474);
#2034=LINE('',#10699,#2475);
#2035=LINE('',#10711,#2476);
#2036=LINE('',#10715,#2477);
#2037=LINE('',#10719,#2478);
#2038=LINE('',#10726,#2479);
#2039=LINE('',#10728,#2480);
#2458=VECTOR('',#8592,1.);
#2459=VECTOR('',#8593,1.);
#2460=VECTOR('',#8594,1.);
#2461=VECTOR('',#8595,1.);
#2462=VECTOR('',#8598,1.);
#2463=VECTOR('',#8599,1.);
#2464=VECTOR('',#8600,1.);
#2465=VECTOR('',#8603,1.);
#2466=VECTOR('',#8604,1.);
#2467=VECTOR('',#8605,1.);
#2468=VECTOR('',#8608,1.);
#2469=VECTOR('',#8609,1.);
#2470=VECTOR('',#8610,1.);
#2471=VECTOR('',#8613,1.);
#2472=VECTOR('',#8614,1.);
#2473=VECTOR('',#8615,1.);
#2474=VECTOR('',#8618,1.);
#2475=VECTOR('',#8619,1.);
#2476=VECTOR('',#8636,0.4);
#2477=VECTOR('',#8641,0.425);
#2478=VECTOR('',#8646,0.41);
#2479=VECTOR('',#8655,0.26);
#2480=VECTOR('',#8658,0.25);
#2849=CIRCLE('',#7313,0.24505);
#2850=CIRCLE('',#7315,0.375);
#2851=CIRCLE('',#7317,0.425);
#2852=CIRCLE('',#7319,0.425);
#2853=CIRCLE('',#7321,0.395);
#2854=CIRCLE('',#7323,0.27);
#2855=CIRCLE('',#7325,0.24505);
#3262=VERTEX_POINT('',#10665);
#3263=VERTEX_POINT('',#10666);
#3264=VERTEX_POINT('',#10668);
#3265=VERTEX_POINT('',#10670);
#3266=VERTEX_POINT('',#10674);
#3267=VERTEX_POINT('',#10676);
#3268=VERTEX_POINT('',#10680);
#3269=VERTEX_POINT('',#10682);
#3270=VERTEX_POINT('',#10686);
#3271=VERTEX_POINT('',#10688);
#3272=VERTEX_POINT('',#10692);
#3273=VERTEX_POINT('',#10694);
#3274=VERTEX_POINT('',#10703);
#3275=VERTEX_POINT('',#10706);
#3276=VERTEX_POINT('',#10709);
#3277=VERTEX_POINT('',#10713);
#3278=VERTEX_POINT('',#10717);
#3279=VERTEX_POINT('',#10721);
#3280=VERTEX_POINT('',#10724);
#3897=EDGE_CURVE('',#3262,#3263,#2017,.T.);
#3898=EDGE_CURVE('',#3263,#3264,#2018,.T.);
#3899=EDGE_CURVE('',#3264,#3265,#2019,.T.);
#3900=EDGE_CURVE('',#3262,#3265,#2020,.T.);
#3901=EDGE_CURVE('',#3263,#3266,#2021,.T.);
#3902=EDGE_CURVE('',#3266,#3267,#2022,.T.);
#3903=EDGE_CURVE('',#3267,#3264,#2023,.T.);
#3904=EDGE_CURVE('',#3266,#3268,#2024,.T.);
#3905=EDGE_CURVE('',#3268,#3269,#2025,.T.);
#3906=EDGE_CURVE('',#3269,#3267,#2026,.T.);
#3907=EDGE_CURVE('',#3268,#3270,#2027,.T.);
#3908=EDGE_CURVE('',#3270,#3271,#2028,.T.);
#3909=EDGE_CURVE('',#3271,#3269,#2029,.T.);
#3910=EDGE_CURVE('',#3270,#3272,#2030,.T.);
#3911=EDGE_CURVE('',#3272,#3273,#2031,.T.);
#3912=EDGE_CURVE('',#3273,#3271,#2032,.T.);
#3913=EDGE_CURVE('',#3272,#3262,#2033,.T.);
#3914=EDGE_CURVE('',#3265,#3273,#2034,.T.);
#3915=EDGE_CURVE('',#3274,#3274,#2849,.T.);
#3916=EDGE_CURVE('',#3275,#3275,#2850,.T.);
#3917=EDGE_CURVE('',#3276,#3276,#2851,.T.);
#3918=EDGE_CURVE('',#3276,#3275,#2035,.T.);
#3919=EDGE_CURVE('',#3277,#3277,#2852,.T.);
#3920=EDGE_CURVE('',#3277,#3276,#2036,.T.);
#3921=EDGE_CURVE('',#3278,#3278,#2853,.T.);
#3922=EDGE_CURVE('',#3278,#3277,#2037,.T.);
#3923=EDGE_CURVE('',#3279,#3279,#2854,.T.);
#3924=EDGE_CURVE('',#3280,#3280,#2855,.F.);
#3925=EDGE_CURVE('',#3280,#3279,#2038,.T.);
#3926=EDGE_CURVE('',#3274,#3280,#2039,.T.);
#4985=ORIENTED_EDGE('',*,*,#3897,.T.);
#4986=ORIENTED_EDGE('',*,*,#3898,.T.);
#4987=ORIENTED_EDGE('',*,*,#3899,.T.);
#4988=ORIENTED_EDGE('',*,*,#3900,.F.);
#4989=ORIENTED_EDGE('',*,*,#3901,.T.);
#4990=ORIENTED_EDGE('',*,*,#3902,.T.);
#4991=ORIENTED_EDGE('',*,*,#3903,.T.);
#4992=ORIENTED_EDGE('',*,*,#3898,.F.);
#4993=ORIENTED_EDGE('',*,*,#3904,.T.);
#4994=ORIENTED_EDGE('',*,*,#3905,.T.);
#4995=ORIENTED_EDGE('',*,*,#3906,.T.);
#4996=ORIENTED_EDGE('',*,*,#3902,.F.);
#4997=ORIENTED_EDGE('',*,*,#3907,.T.);
#4998=ORIENTED_EDGE('',*,*,#3908,.T.);
#4999=ORIENTED_EDGE('',*,*,#3909,.T.);
#5000=ORIENTED_EDGE('',*,*,#3905,.F.);
#5001=ORIENTED_EDGE('',*,*,#3910,.T.);
#5002=ORIENTED_EDGE('',*,*,#3911,.T.);
#5003=ORIENTED_EDGE('',*,*,#3912,.T.);
#5004=ORIENTED_EDGE('',*,*,#3908,.F.);
#5005=ORIENTED_EDGE('',*,*,#3913,.T.);
#5006=ORIENTED_EDGE('',*,*,#3900,.T.);
#5007=ORIENTED_EDGE('',*,*,#3914,.T.);
#5008=ORIENTED_EDGE('',*,*,#3911,.F.);
#5009=ORIENTED_EDGE('',*,*,#3913,.F.);
#5010=ORIENTED_EDGE('',*,*,#3910,.F.);
#5011=ORIENTED_EDGE('',*,*,#3907,.F.);
#5012=ORIENTED_EDGE('',*,*,#3904,.F.);
#5013=ORIENTED_EDGE('',*,*,#3901,.F.);
#5014=ORIENTED_EDGE('',*,*,#3897,.F.);
#5015=ORIENTED_EDGE('',*,*,#3914,.F.);
#5016=ORIENTED_EDGE('',*,*,#3899,.F.);
#5017=ORIENTED_EDGE('',*,*,#3903,.F.);
#5018=ORIENTED_EDGE('',*,*,#3906,.F.);
#5019=ORIENTED_EDGE('',*,*,#3909,.F.);
#5020=ORIENTED_EDGE('',*,*,#3912,.F.);
#5021=ORIENTED_EDGE('',*,*,#3915,.F.);
#5022=ORIENTED_EDGE('',*,*,#3916,.F.);
#5023=ORIENTED_EDGE('',*,*,#3917,.F.);
#5024=ORIENTED_EDGE('',*,*,#3918,.T.);
#5025=ORIENTED_EDGE('',*,*,#3916,.T.);
#5026=ORIENTED_EDGE('',*,*,#3918,.F.);
#5027=ORIENTED_EDGE('',*,*,#3919,.F.);
#5028=ORIENTED_EDGE('',*,*,#3920,.T.);
#5029=ORIENTED_EDGE('',*,*,#3917,.T.);
#5030=ORIENTED_EDGE('',*,*,#3920,.F.);
#5031=ORIENTED_EDGE('',*,*,#3921,.F.);
#5032=ORIENTED_EDGE('',*,*,#3922,.T.);
#5033=ORIENTED_EDGE('',*,*,#3919,.T.);
#5034=ORIENTED_EDGE('',*,*,#3922,.F.);
#5035=ORIENTED_EDGE('',*,*,#3921,.T.);
#5036=ORIENTED_EDGE('',*,*,#3923,.F.);
#5037=ORIENTED_EDGE('',*,*,#3924,.F.);
#5038=ORIENTED_EDGE('',*,*,#3925,.T.);
#5039=ORIENTED_EDGE('',*,*,#3923,.T.);
#5040=ORIENTED_EDGE('',*,*,#3925,.F.);
#5041=ORIENTED_EDGE('',*,*,#3915,.T.);
#5042=ORIENTED_EDGE('',*,*,#3926,.T.);
#5043=ORIENTED_EDGE('',*,*,#3924,.T.);
#5044=ORIENTED_EDGE('',*,*,#3926,.F.);
#6091=CYLINDRICAL_SURFACE('',#7318,0.425);
#6092=CYLINDRICAL_SURFACE('',#7326,0.24505);
#6298=ADVANCED_FACE('',(#1023),#728,.F.);
#6299=ADVANCED_FACE('',(#1024),#729,.F.);
#6300=ADVANCED_FACE('',(#1025),#730,.F.);
#6301=ADVANCED_FACE('',(#1026),#731,.F.);
#6302=ADVANCED_FACE('',(#1027),#732,.F.);
#6303=ADVANCED_FACE('',(#1028),#733,.F.);
#6304=ADVANCED_FACE('',(#1029),#734,.F.);
#6305=ADVANCED_FACE('',(#1030),#735,.F.);
#6306=ADVANCED_FACE('',(#1031),#736,.F.);
#6307=ADVANCED_FACE('',(#1032),#737,.T.);
#6308=ADVANCED_FACE('',(#1033),#305,.T.);
#6309=ADVANCED_FACE('',(#1034),#6091,.T.);
#6310=ADVANCED_FACE('',(#1035),#306,.T.);
#6311=ADVANCED_FACE('',(#1036,#587),#738,.T.);
#6312=ADVANCED_FACE('',(#1037),#307,.T.);
#6313=ADVANCED_FACE('',(#1038),#6092,.T.);
#6580=CLOSED_SHELL('',(#6298,#6299,#6300,#6301,#6302,#6303,#6304,#6305));
#6581=CLOSED_SHELL('',(#6306,#6307,#6308,#6309,#6310,#6311,#6312,#6313));
#7303=AXIS2_PLACEMENT_3D('',#10663,#8588,#8589);
#7304=AXIS2_PLACEMENT_3D('',#10664,#8590,#8591);
#7305=AXIS2_PLACEMENT_3D('',#10673,#8596,#8597);
#7306=AXIS2_PLACEMENT_3D('',#10679,#8601,#8602);
#7307=AXIS2_PLACEMENT_3D('',#10685,#8606,#8607);
#7308=AXIS2_PLACEMENT_3D('',#10691,#8611,#8612);
#7309=AXIS2_PLACEMENT_3D('',#10697,#8616,#8617);
#7310=AXIS2_PLACEMENT_3D('',#10700,#8620,#8621);
#7311=AXIS2_PLACEMENT_3D('',#10701,#8622,#8623);
#7312=AXIS2_PLACEMENT_3D('',#10702,#8624,#8625);
#7313=AXIS2_PLACEMENT_3D('',#10704,#8626,#8627);
#7314=AXIS2_PLACEMENT_3D('',#10705,#8628,#8629);
#7315=AXIS2_PLACEMENT_3D('',#10707,#8630,#8631);
#7316=AXIS2_PLACEMENT_3D('',#10708,#8632,#8633);
#7317=AXIS2_PLACEMENT_3D('',#10710,#8634,#8635);
#7318=AXIS2_PLACEMENT_3D('',#10712,#8637,#8638);
#7319=AXIS2_PLACEMENT_3D('',#10714,#8639,#8640);
#7320=AXIS2_PLACEMENT_3D('',#10716,#8642,#8643);
#7321=AXIS2_PLACEMENT_3D('',#10718,#8644,#8645);
#7322=AXIS2_PLACEMENT_3D('',#10720,#8647,#8648);
#7323=AXIS2_PLACEMENT_3D('',#10722,#8649,#8650);
#7324=AXIS2_PLACEMENT_3D('',#10723,#8651,#8652);
#7325=AXIS2_PLACEMENT_3D('',#10725,#8653,#8654);
#7326=AXIS2_PLACEMENT_3D('',#10727,#8656,#8657);
#8588=DIRECTION('axis',(0.,0.,1.));
#8589=DIRECTION('refdir',(1.,0.,0.));
#8590=DIRECTION('center_axis',(0.866025403784439,0.,-0.5));
#8591=DIRECTION('ref_axis',(0.5,0.,0.866025403784439));
#8592=DIRECTION('',(-0.5,0.,-0.866025403784439));
#8593=DIRECTION('',(0.,-1.,0.));
#8594=DIRECTION('',(0.5,0.,0.866025403784439));
#8595=DIRECTION('',(0.,-1.,0.));
#8596=DIRECTION('center_axis',(1.20185167898973E-16,0.,-1.));
#8597=DIRECTION('ref_axis',(1.,0.,1.20185167898973E-16));
#8598=DIRECTION('',(-1.,0.,-1.20185167898973E-16));
#8599=DIRECTION('',(0.,-1.,0.));
#8600=DIRECTION('',(1.,0.,1.20185167898973E-16));
#8601=DIRECTION('center_axis',(-0.866025403784439,0.,-0.5));
#8602=DIRECTION('ref_axis',(0.5,0.,-0.866025403784439));
#8603=DIRECTION('',(-0.5,0.,0.866025403784439));
#8604=DIRECTION('',(0.,-1.,0.));
#8605=DIRECTION('',(0.5,0.,-0.866025403784439));
#8606=DIRECTION('center_axis',(-0.866025403784439,0.,0.5));
#8607=DIRECTION('ref_axis',(-0.5,0.,-0.866025403784439));
#8608=DIRECTION('',(0.5,0.,0.866025403784439));
#8609=DIRECTION('',(0.,-1.,0.));
#8610=DIRECTION('',(-0.5,0.,-0.866025403784439));
#8611=DIRECTION('center_axis',(-2.40370335797945E-16,0.,1.));
#8612=DIRECTION('ref_axis',(-1.,0.,-2.40370335797945E-16));
#8613=DIRECTION('',(1.,0.,2.40370335797945E-16));
#8614=DIRECTION('',(0.,-1.,0.));
#8615=DIRECTION('',(-1.,0.,-2.40370335797945E-16));
#8616=DIRECTION('center_axis',(0.866025403784439,0.,0.5));
#8617=DIRECTION('ref_axis',(-0.5,0.,0.866025403784439));
#8618=DIRECTION('',(0.5,0.,-0.866025403784439));
#8619=DIRECTION('',(-0.5,0.,0.866025403784439));
#8620=DIRECTION('center_axis',(0.,1.,0.));
#8621=DIRECTION('ref_axis',(1.,0.,0.));
#8622=DIRECTION('center_axis',(0.,-1.,0.));
#8623=DIRECTION('ref_axis',(0.,0.,-1.));
#8624=DIRECTION('center_axis',(0.,1.,0.));
#8625=DIRECTION('ref_axis',(1.,0.,0.));
#8626=DIRECTION('center_axis',(0.,1.,0.));
#8627=DIRECTION('ref_axis',(1.,0.,0.));
#8628=DIRECTION('center_axis',(0.,1.,0.));
#8629=DIRECTION('ref_axis',(0.,0.,1.));
#8630=DIRECTION('center_axis',(0.,-1.,0.));
#8631=DIRECTION('ref_axis',(1.,0.,0.));
#8632=DIRECTION('center_axis',(0.,-1.,0.));
#8633=DIRECTION('ref_axis',(1.,0.,0.));
#8634=DIRECTION('center_axis',(0.,-1.,0.));
#8635=DIRECTION('ref_axis',(1.,0.,0.));
#8636=DIRECTION('',(0.707106781186548,0.707106781186547,8.65956056235493E-17));
#8637=DIRECTION('center_axis',(0.,-1.,0.));
#8638=DIRECTION('ref_axis',(1.,0.,0.));
#8639=DIRECTION('center_axis',(0.,-1.,0.));
#8640=DIRECTION('ref_axis',(1.,0.,0.));
#8641=DIRECTION('',(0.,1.,0.));
#8642=DIRECTION('center_axis',(0.,1.,0.));
#8643=DIRECTION('ref_axis',(1.,0.,0.));
#8644=DIRECTION('center_axis',(0.,-1.,0.));
#8645=DIRECTION('ref_axis',(1.,0.,0.));
#8646=DIRECTION('',(-0.707106781186547,0.707106781186548,-8.65956056235493E-17));
#8647=DIRECTION('center_axis',(0.,-1.,0.));
#8648=DIRECTION('ref_axis',(0.,0.,-1.));
#8649=DIRECTION('center_axis',(0.,-1.,0.));
#8650=DIRECTION('ref_axis',(1.,0.,0.));
#8651=DIRECTION('center_axis',(0.,1.,0.));
#8652=DIRECTION('ref_axis',(1.,0.,0.));
#8653=DIRECTION('center_axis',(0.,1.,0.));
#8654=DIRECTION('ref_axis',(1.,0.,0.));
#8655=DIRECTION('',(-0.447213595499958,0.894427190999916,-5.47678698264203E-17));
#8656=DIRECTION('center_axis',(0.,-1.,0.));
#8657=DIRECTION('ref_axis',(1.,0.,0.));
#8658=DIRECTION('',(0.,1.,0.));
#10663=CARTESIAN_POINT('',(0.,0.,0.));
#10664=CARTESIAN_POINT('Origin',(0.115470053837925,-0.5,-0.2));
#10665=CARTESIAN_POINT('',(0.23094010767585,-0.5,0.));
#10666=CARTESIAN_POINT('',(0.115470053837925,-0.5,-0.2));
#10667=CARTESIAN_POINT('',(0.23094010767585,-0.5,0.));
#10668=CARTESIAN_POINT('',(0.115470053837925,-0.8,-0.2));
#10669=CARTESIAN_POINT('',(0.115470053837925,-0.5,-0.2));
#10670=CARTESIAN_POINT('',(0.23094010767585,-0.8,0.));
#10671=CARTESIAN_POINT('',(0.23094010767585,-0.8,0.));
#10672=CARTESIAN_POINT('',(0.23094010767585,-0.5,0.));
#10673=CARTESIAN_POINT('Origin',(-0.115470053837925,-0.5,-0.2));
#10674=CARTESIAN_POINT('',(-0.115470053837925,-0.5,-0.2));
#10675=CARTESIAN_POINT('',(0.115470053837925,-0.5,-0.2));
#10676=CARTESIAN_POINT('',(-0.115470053837925,-0.8,-0.2));
#10677=CARTESIAN_POINT('',(-0.115470053837925,-0.5,-0.2));
#10678=CARTESIAN_POINT('',(0.115470053837925,-0.8,-0.2));
#10679=CARTESIAN_POINT('Origin',(-0.23094010767585,-0.5,-2.77555756156289E-17));
#10680=CARTESIAN_POINT('',(-0.23094010767585,-0.5,-2.82820063659975E-17));
#10681=CARTESIAN_POINT('',(-0.115470053837925,-0.5,-0.2));
#10682=CARTESIAN_POINT('',(-0.23094010767585,-0.8,-2.77555756156289E-17));
#10683=CARTESIAN_POINT('',(-0.23094010767585,-0.5,-2.82820063659975E-17));
#10684=CARTESIAN_POINT('',(-0.115470053837925,-0.8,-0.2));
#10685=CARTESIAN_POINT('Origin',(-0.115470053837925,-0.5,0.2));
#10686=CARTESIAN_POINT('',(-0.115470053837925,-0.5,0.2));
#10687=CARTESIAN_POINT('',(-0.23094010767585,-0.5,-2.82820063659975E-17));
#10688=CARTESIAN_POINT('',(-0.115470053837925,-0.8,0.2));
#10689=CARTESIAN_POINT('',(-0.115470053837925,-0.5,0.2));
#10690=CARTESIAN_POINT('',(-0.23094010767585,-0.8,-2.82820063659975E-17));
#10691=CARTESIAN_POINT('Origin',(0.115470053837925,-0.5,0.2));
#10692=CARTESIAN_POINT('',(0.115470053837925,-0.5,0.2));
#10693=CARTESIAN_POINT('',(-0.115470053837925,-0.5,0.2));
#10694=CARTESIAN_POINT('',(0.115470053837925,-0.8,0.2));
#10695=CARTESIAN_POINT('',(0.115470053837925,-0.5,0.2));
#10696=CARTESIAN_POINT('',(-0.115470053837925,-0.8,0.2));
#10697=CARTESIAN_POINT('Origin',(0.23094010767585,-0.5,0.));
#10698=CARTESIAN_POINT('',(0.115470053837925,-0.5,0.2));
#10699=CARTESIAN_POINT('',(0.115470053837925,-0.8,0.2));
#10700=CARTESIAN_POINT('Origin',(0.,-0.5,0.));
#10701=CARTESIAN_POINT('Origin',(0.,-0.8,0.));
#10702=CARTESIAN_POINT('Origin',(0.,-1.4,0.));
#10703=CARTESIAN_POINT('',(-0.24505,-1.4,3.00099698131059E-17));
#10704=CARTESIAN_POINT('Origin',(0.,-1.4,0.));
#10705=CARTESIAN_POINT('Origin',(0.375,0.5,0.));
#10706=CARTESIAN_POINT('',(-0.375,0.5,-4.59242549680257E-17));
#10707=CARTESIAN_POINT('Origin',(0.,0.5,0.));
#10708=CARTESIAN_POINT('Origin',(0.,0.475,0.));
#10709=CARTESIAN_POINT('',(-0.425,0.45,-5.20474889637625E-17));
#10710=CARTESIAN_POINT('Origin',(0.,0.45,0.));
#10711=CARTESIAN_POINT('',(-0.4,0.475,-4.89858719658941E-17));
#10712=CARTESIAN_POINT('Origin',(0.,0.24,0.));
#10713=CARTESIAN_POINT('',(-0.425,0.0299999999999998,-5.20474889637625E-17));
#10714=CARTESIAN_POINT('Origin',(0.,0.0299999999999998,0.));
#10715=CARTESIAN_POINT('',(-0.425,0.24,-5.20474889637625E-17));
#10716=CARTESIAN_POINT('Origin',(0.,0.0150000000000001,0.));
#10717=CARTESIAN_POINT('',(-0.395,4.85722573273506E-17,-4.83735485663204E-17));
#10718=CARTESIAN_POINT('Origin',(0.,0.,0.));
#10719=CARTESIAN_POINT('',(-0.41,0.0150000000000001,-5.02105187650415E-17));
#10720=CARTESIAN_POINT('Origin',(0.27,0.,0.));
#10721=CARTESIAN_POINT('',(-0.27,0.,-3.30654635769785E-17));
#10722=CARTESIAN_POINT('Origin',(0.,0.,0.));
#10723=CARTESIAN_POINT('Origin',(0.,-0.02,0.));
#10724=CARTESIAN_POINT('',(-0.24505,-0.0498999999999999,3.00099698131059E-17));
#10725=CARTESIAN_POINT('Origin',(0.,-0.0498999999999999,0.));
#10726=CARTESIAN_POINT('',(-0.26,-0.02,-3.18408167778312E-17));
#10727=CARTESIAN_POINT('Origin',(0.,-0.995,0.));
#10728=CARTESIAN_POINT('',(-0.24505,-0.995,-3.00099698131059E-17));
#12335=UNCERTAINTY_MEASURE_WITH_UNIT(LENGTH_MEASURE(0.001),#12414,
'DISTANCE_ACCURACY_VALUE',
'Maximum model space distance between geometric entities at asserted c
onnectivities');
#12367=UNCERTAINTY_MEASURE_WITH_UNIT(LENGTH_MEASURE(0.001),#12414,
'DISTANCE_ACCURACY_VALUE',
'Maximum model space distance between geometric entities at asserted c
onnectivities');
#12381=(
GEOMETRIC_REPRESENTATION_CONTEXT(3)
GLOBAL_UNCERTAINTY_ASSIGNED_CONTEXT((#12335))
GLOBAL_UNIT_ASSIGNED_CONTEXT((#12414,#12416,#12417))
REPRESENTATION_CONTEXT('','3D')
);
#12413=(
GEOMETRIC_REPRESENTATION_CONTEXT(3)
GLOBAL_UNCERTAINTY_ASSIGNED_CONTEXT((#12367))
GLOBAL_UNIT_ASSIGNED_CONTEXT((#12414,#12416,#12417))
REPRESENTATION_CONTEXT('','3D')
);
#12414=(
LENGTH_UNIT()
NAMED_UNIT(*)
SI_UNIT(.CENTI.,.METRE.)
);
#12416=(
NAMED_UNIT(*)
PLANE_ANGLE_UNIT()
SI_UNIT($,.RADIAN.)
);
#12417=(
NAMED_UNIT(*)
SI_UNIT($,.STERADIAN.)
SOLID_ANGLE_UNIT()
);
#12431=SHAPE_DEFINITION_REPRESENTATION(#12476,#12584);
#12476=PRODUCT_DEFINITION_SHAPE('',$,#12630);
#12584=SHAPE_REPRESENTATION('',(#7303),#12381);
#12616=PRODUCT_DEFINITION_CONTEXT('part definition',#12753,'design');
#12630=PRODUCT_DEFINITION('M5x14 Cap Screw','M5x14 Cap Screw',#12675,#12616);
#12675=PRODUCT_DEFINITION_FORMATION('',$,#12768);
#12753=APPLICATION_CONTEXT(
'Core Data for Automotive Mechanical Design Process');
#12754=PRODUCT_CONTEXT('part definition',#12753,'mechanical');
#12768=PRODUCT('M5x14 Cap Screw','M5x14 Cap Screw','M5x14 Cap Screw',(#12754));
#12870=COLOUR_RGB('Black',0.12,0.14,0.17);
#12871=FILL_AREA_STYLE_COLOUR('',#12870);
#12872=FILL_AREA_STYLE('',(#12871));
#12873=SURFACE_STYLE_FILL_AREA(#12872);
#12874=SURFACE_SIDE_STYLE('',(#12873));
#12875=SURFACE_STYLE_USAGE(.BOTH.,#12874);
#12876=PRESENTATION_STYLE_ASSIGNMENT((#12875));
ENDSEC;
END-ISO-10303-21;
